ISO-10303-21;
HEADER;
/* Generated by software containing ST-Developer
 * from STEP Tools, Inc. (www.steptools.com) 
 */

FILE_DESCRIPTION(
/* description */ ('Hand-crank gear train demonstrator'),
/* implementation_level */ '2;1');

FILE_NAME(
/* name */ 'Flat Washer - M6.step',
/* time_stamp */ '2026-10-28T03:22:13-07:00',
/* author */ (''),
/* organization */ (''),
/* preprocessor_version */ 'ST-DEVELOPER v20.2',
/* originating_system */ 'Autodesk Translation Framework v15.17.0.0',
/* authorisation */ '');

FILE_SCHEMA (('AUTOMOTIVE_DESIGN { 1 0 10303 214 3 1 1 }'));
ENDSEC;

DATA;
#10=MECHANICAL_DESIGN_GEOMETRIC_PRESENTATION_REPRESENTATION('',(#1241),#62758);
#1098=SHAPE_REPRESENTATION_RELATIONSHIP('SRR','None',#63073,#1162);
#1162=ADVANCED_BREP_SHAPE_REPRESENTATION('',(#1317),#62727);
#1241=STYLED_ITEM('',(#63469),#1317);
#1317=MANIFOLD_SOLID_BREP('Body1',#16424);
#1568=FACE_BOUND('',#3775,.T.);
#1569=FACE_BOUND('',#3777,.T.);
#1923=PLANE('',#18105);
#1924=PLANE('',#18106);
#2610=FACE_OUTER_BOUND('',#3772,.T.);
#2611=FACE_OUTER_BOUND('',#3773,.T.);
#2612=FACE_OUTER_BOUND('',#3774,.T.);
#2613=FACE_OUTER_BOUND('',#3776,.T.);
#3772=EDGE_LOOP('',(#12945,#12946,#12947,#12948));
#3773=EDGE_LOOP('',(#12949,#12950,#12951,#12952));
#3774=EDGE_LOOP('',(#12953));
#3775=EDGE_LOOP('',(#12954));
#3776=EDGE_LOOP('',(#12955));
#3777=EDGE_LOOP('',(#12956));
#4904=LINE('',#26310,#6036);
#4905=LINE('',#26316,#6037);
#6036=VECTOR('',#21335,0.32);
#6037=VECTOR('',#21342,0.6);
#6951=CIRCLE('',#18100,0.32);
#6952=CIRCLE('',#18101,0.32);
#6953=CIRCLE('',#18103,0.6);
#6954=CIRCLE('',#18104,0.6);
#7930=VERTEX_POINT('',#26307);
#7931=VERTEX_POINT('',#26309);
#7932=VERTEX_POINT('',#26313);
#7933=VERTEX_POINT('',#26315);
#9724=EDGE_CURVE('',#7930,#7930,#6951,.T.);
#9725=EDGE_CURVE('',#7930,#7931,#4904,.T.);
#9726=EDGE_CURVE('',#7931,#7931,#6952,.T.);
#9727=EDGE_CURVE('',#7932,#7932,#6953,.T.);
#9728=EDGE_CURVE('',#7932,#7933,#4905,.T.);
#9729=EDGE_CURVE('',#7933,#7933,#6954,.T.);
#12945=ORIENTED_EDGE('',*,*,#9724,.F.);
#12946=ORIENTED_EDGE('',*,*,#9725,.T.);
#12947=ORIENTED_EDGE('',*,*,#9726,.T.);
#12948=ORIENTED_EDGE('',*,*,#9725,.F.);
#12949=ORIENTED_EDGE('',*,*,#9727,.F.);
#12950=ORIENTED_EDGE('',*,*,#9728,.T.);
#12951=ORIENTED_EDGE('',*,*,#9729,.T.);
#12952=ORIENTED_EDGE('',*,*,#9728,.F.);
#12953=ORIENTED_EDGE('',*,*,#9727,.T.);
#12954=ORIENTED_EDGE('',*,*,#9724,.T.);
#12955=ORIENTED_EDGE('',*,*,#9729,.F.);
#12956=ORIENTED_EDGE('',*,*,#9726,.F.);
#15313=CYLINDRICAL_SURFACE('',#18099,0.32);
#15314=CYLINDRICAL_SURFACE('',#18102,0.6);
#15920=ADVANCED_FACE('',(#2610),#15313,.F.);
#15921=ADVANCED_FACE('',(#2611),#15314,.T.);
#15922=ADVANCED_FACE('',(#2612,#1568),#1923,.T.);
#15923=ADVANCED_FACE('',(#2613,#1569),#1924,.F.);
#16424=CLOSED_SHELL('',(#15920,#15921,#15922,#15923));
#18098=AXIS2_PLACEMENT_3D('',#26305,#21329,#21330);
#18099=AXIS2_PLACEMENT_3D('',#26306,#21331,#21332);
#18100=AXIS2_PLACEMENT_3D('',#26308,#21333,#21334);
#18101=AXIS2_PLACEMENT_3D('',#26311,#21336,#21337);
#18102=AXIS2_PLACEMENT_3D('',#26312,#21338,#21339);
#18103=AXIS2_PLACEMENT_3D('',#26314,#21340,#21341);
#18104=AXIS2_PLACEMENT_3D('',#26317,#21343,#21344);
#18105=AXIS2_PLACEMENT_3D('',#26318,#21345,#21346);
#18106=AXIS2_PLACEMENT_3D('',#26319,#21347,#21348);
#21329=DIRECTION('axis',(0.,0.,1.));
#21330=DIRECTION('refdir',(1.,0.,0.));
#21331=DIRECTION('center_axis',(0.,1.,0.));
#21332=DIRECTION('ref_axis',(1.,0.,0.));
#21333=DIRECTION('center_axis',(0.,-1.,0.));
#21334=DIRECTION('ref_axis',(1.,0.,0.));
#21335=DIRECTION('',(0.,-1.,0.));
#21336=DIRECTION('center_axis',(0.,-1.,0.));
#21337=DIRECTION('ref_axis',(1.,0.,0.));
#21338=DIRECTION('center_axis',(0.,1.,0.));
#21339=DIRECTION('ref_axis',(1.,0.,0.));
#21340=DIRECTION('center_axis',(0.,1.,0.));
#21341=DIRECTION('ref_axis',(1.,0.,0.));
#21342=DIRECTION('',(0.,-1.,0.));
#21343=DIRECTION('center_axis',(0.,1.,0.));
#21344=DIRECTION('ref_axis',(1.,0.,0.));
#21345=DIRECTION('center_axis',(0.,1.,0.));
#21346=DIRECTION('ref_axis',(1.,0.,0.));
#21347=DIRECTION('center_axis',(0.,1.,0.));
#21348=DIRECTION('ref_axis',(1.,0.,0.));
#26305=CARTESIAN_POINT('',(0.,0.,0.));
#26306=CARTESIAN_POINT('Origin',(0.,0.,0.));
#26307=CARTESIAN_POINT('',(-0.32,0.16,3.91886975727153E-17));
#26308=CARTESIAN_POINT('Origin',(0.,0.16,0.));
#26309=CARTESIAN_POINT('',(-0.32,0.,3.91886975727153E-17));
#26310=CARTESIAN_POINT('',(-0.32,0.,3.91886975727153E-17));
#26311=CARTESIAN_POINT('Origin',(0.,0.,0.));
#26312=CARTESIAN_POINT('Origin',(0.,0.,0.));
#26313=CARTESIAN_POINT('',(-0.6,0.16,7.34788079488412E-17));
#26314=CARTESIAN_POINT('Origin',(0.,0.16,0.));
#26315=CARTESIAN_POINT('',(-0.6,0.,7.34788079488412E-17));
#26316=CARTESIAN_POINT('',(-0.6,0.,7.34788079488412E-17));
#26317=CARTESIAN_POINT('Origin',(0.,0.,0.));
#26318=CARTESIAN_POINT('Origin',(0.,0.16,0.));
#26319=CARTESIAN_POINT('Origin',(0.,0.,0.));
#62653=UNCERTAINTY_MEASURE_WITH_UNIT(LENGTH_MEASURE(0.001),#62759,
'DISTANCE_ACCURACY_VALUE',
'Maximum model space distance between geometric entities at asserted c
onnectivities');
#62684=UNCERTAINTY_MEASURE_WITH_UNIT(LENGTH_MEASURE(0.001),#62759,
'DISTANCE_ACCURACY_VALUE',
'Maximum model space distance between geometric entities at asserted c
onnectivities');
#62727=(
GEOMETRIC_REPRESENTATION_CONTEXT(3)
GLOBAL_UNCERTAINTY_ASSIGNED_CONTEXT((#62653))
GLOBAL_UNIT_ASSIGNED_CONTEXT((#62759,#62761,#62762))
REPRESENTATION_CONTEXT('','3D')
);
#62758=(
GEOMETRIC_REPRESENTATION_CONTEXT(3)
GLOBAL_UNCERTAINTY_ASSIGNED_CONTEXT((#62684))
GLOBAL_UNIT_ASSIGNED_CONTEXT((#62759,#62761,#62762))
REPRESENTATION_CONTEXT('','3D')
);
#62759=(
LENGTH_UNIT()
NAMED_UNIT(*)
SI_UNIT(.CENTI.,.METRE.)
);
#62761=(
NAMED_UNIT(*)
PLANE_ANGLE_UNIT()
SI_UNIT($,.RADIAN.)
);
#62762=(
NAMED_UNIT(*)
SI_UNIT($,.STERADIAN.)
SOLID_ANGLE_UNIT()
);
#62805=SHAPE_DEFINITION_REPRESENTATION(#62888,#63073);
#62888=PRODUCT_DEFINITION_SHAPE('',$,#63147);
#63073=SHAPE_REPRESENTATION('',(#18098),#62727);
#63104=PRODUCT_DEFINITION_CONTEXT('part definition',#63325,'design');
#63147=PRODUCT_DEFINITION('Flat Washer - M6','Flat Washer - M6',#63220,
#63104);
#63220=PRODUCT_DEFINITION_FORMATION('',$,#63369);
#63325=APPLICATION_CONTEXT(
'Core Data for Automotive Mechanical Design Process');
#63326=PRODUCT_CONTEXT('part definition',#63325,'mechanical');
#63369=PRODUCT('Flat Washer - M6','Flat Washer - M6','Flat Washer - M6',
(#63326));
#63463=COLOUR_RGB('Black',0.12,0.14,0.17);
#63464=FILL_AREA_STYLE_COLOUR('',#63463);
#63465=FILL_AREA_STYLE('',(#63464));
#63466=SURFACE_STYLE_FILL_AREA(#63465);
#63467=SURFACE_SIDE_STYLE('',(#63466));
#63468=SURFACE_STYLE_USAGE(.BOTH.,#63467);
#63469=PRESENTATION_STYLE_ASSIGNMENT((#63468));
ENDSEC;
END-ISO-10303-21;
